ISO-10303-21;
HEADER;
/* Generated by software containing ST-Developer
 * from STEP Tools, Inc. (www.steptools.com) 
 */

FILE_DESCRIPTION(
/* description */ (''),
/* implementation_level */ '2;1');

FILE_NAME(
/* name */ 'Left_Rod.step',
/* time_stamp */ '2026-10-19T01:30:23+06:00',
/* author */ (''),
/* organization */ (''),
/* preprocessor_version */ 'ST-DEVELOPER v20.2',
/* originating_system */ 'Autodesk Translation Framework v15.15.0.0',
/* authorisation */ '');

FILE_SCHEMA (('AUTOMOTIVE_DESIGN { 1 0 10303 214 3 1 1 }'));
ENDSEC;

DATA;
#10=MECHANICAL_DESIGN_GEOMETRIC_PRESENTATION_REPRESENTATION('',(#93),#10639);
#73=SHAPE_REPRESENTATION_RELATIONSHIP('SRR','None',#10683,#83);
#83=ADVANCED_BREP_SHAPE_REPRESENTATION('',(#103),#10635);
#93=STYLED_ITEM('',(#10790),#103);
#103=MANIFOLD_SOLID_BREP('Left_Rod',#5719);
#361=PLANE('',#6453);
#362=PLANE('',#6457);
#662=FACE_OUTER_BOUND('',#1086,.T.);
#663=FACE_OUTER_BOUND('',#1087,.T.);
#664=FACE_OUTER_BOUND('',#1088,.T.);
#1086=EDGE_LOOP('',(#4708));
#1087=EDGE_LOOP('',(#4709,#4710,#4711,#4712));
#1088=EDGE_LOOP('',(#4713));
#1442=LINE('',#10053,#1772);
#1772=VECTOR('',#8180,4.);
#2180=CIRCLE('',#6454,4.);
#2181=CIRCLE('',#6456,4.);
#2630=VERTEX_POINT('',#10048);
#2631=VERTEX_POINT('',#10051);
#3330=EDGE_CURVE('',#2630,#2630,#2180,.T.);
#3331=EDGE_CURVE('',#2631,#2631,#2181,.T.);
#3332=EDGE_CURVE('',#2631,#2630,#1442,.T.);
#4708=ORIENTED_EDGE('',*,*,#3330,.F.);
#4709=ORIENTED_EDGE('',*,*,#3331,.T.);
#4710=ORIENTED_EDGE('',*,*,#3332,.T.);
#4711=ORIENTED_EDGE('',*,*,#3330,.T.);
#4712=ORIENTED_EDGE('',*,*,#3332,.F.);
#4713=ORIENTED_EDGE('',*,*,#3331,.F.);
#5276=CYLINDRICAL_SURFACE('',#6455,4.);
#5605=ADVANCED_FACE('',(#662),#361,.F.);
#5606=ADVANCED_FACE('',(#663),#5276,.T.);
#5607=ADVANCED_FACE('',(#664),#362,.T.);
#5719=CLOSED_SHELL('',(#5605,#5606,#5607));
#6452=AXIS2_PLACEMENT_3D('',#10046,#8170,#8171);
#6453=AXIS2_PLACEMENT_3D('',#10047,#8172,#8173);
#6454=AXIS2_PLACEMENT_3D('',#10049,#8174,#8175);
#6455=AXIS2_PLACEMENT_3D('',#10050,#8176,#8177);
#6456=AXIS2_PLACEMENT_3D('',#10052,#8178,#8179);
#6457=AXIS2_PLACEMENT_3D('',#10054,#8181,#8182);
#8170=DIRECTION('axis',(0.,0.,1.));
#8171=DIRECTION('refdir',(1.,0.,0.));
#8172=DIRECTION('center_axis',(1.,0.,0.));
#8173=DIRECTION('ref_axis',(0.,1.,0.));
#8174=DIRECTION('center_axis',(1.,0.,0.));
#8175=DIRECTION('ref_axis',(0.,1.,0.));
#8176=DIRECTION('center_axis',(-1.,0.,0.));
#8177=DIRECTION('ref_axis',(0.,1.,0.));
#8178=DIRECTION('center_axis',(-1.,0.,0.));
#8179=DIRECTION('ref_axis',(0.,1.,0.));
#8180=DIRECTION('',(-1.,0.,0.));
#8181=DIRECTION('center_axis',(1.,0.,0.));
#8182=DIRECTION('ref_axis',(0.,1.,0.));
#10046=CARTESIAN_POINT('',(0.,0.,0.));
#10047=CARTESIAN_POINT('Origin',(-145.,21.9999999999999,-1.92966607280848));
#10048=CARTESIAN_POINT('',(-145.,17.9999999999999,-1.92966607280848));
#10049=CARTESIAN_POINT('Origin',(-145.,21.9999999999999,-1.92966607280848));
#10050=CARTESIAN_POINT('Origin',(-125.,21.9999999999999,-1.92966607280848));
#10051=CARTESIAN_POINT('',(145.,17.9999999999999,-1.92966607280848));
#10052=CARTESIAN_POINT('Origin',(145.,21.9999999999999,-1.92966607280848));
#10053=CARTESIAN_POINT('',(-125.,17.9999999999999,-1.92966607280848));
#10054=CARTESIAN_POINT('Origin',(145.,21.9999999999999,-1.92966607280848));
#10623=UNCERTAINTY_MEASURE_WITH_UNIT(LENGTH_MEASURE(0.01),#10640,
'DISTANCE_ACCURACY_VALUE',
'Maximum model space distance between geometric entities at asserted c
onnectivities');
#10627=UNCERTAINTY_MEASURE_WITH_UNIT(LENGTH_MEASURE(0.01),#10640,
'DISTANCE_ACCURACY_VALUE',
'Maximum model space distance between geometric entities at asserted c
onnectivities');
#10635=(
GEOMETRIC_REPRESENTATION_CONTEXT(3)
GLOBAL_UNCERTAINTY_ASSIGNED_CONTEXT((#10623))
GLOBAL_UNIT_ASSIGNED_CONTEXT((#10640,#10642,#10643))
REPRESENTATION_CONTEXT('','3D')
);
#10639=(
GEOMETRIC_REPRESENTATION_CONTEXT(3)
GLOBAL_UNCERTAINTY_ASSIGNED_CONTEXT((#10627))
GLOBAL_UNIT_ASSIGNED_CONTEXT((#10640,#10642,#10643))
REPRESENTATION_CONTEXT('','3D')
);
#10640=(
LENGTH_UNIT()
NAMED_UNIT(*)
SI_UNIT(.MILLI.,.METRE.)
);
#10642=(
NAMED_UNIT(*)
PLANE_ANGLE_UNIT()
SI_UNIT($,.RADIAN.)
);
#10643=(
NAMED_UNIT(*)
SI_UNIT($,.STERADIAN.)
SOLID_ANGLE_UNIT()
);
#10651=SHAPE_DEFINITION_REPRESENTATION(#10662,#10683);
#10662=PRODUCT_DEFINITION_SHAPE('',$,#10695);
#10683=SHAPE_REPRESENTATION('',(#6452),#10635);
#10687=PRODUCT_DEFINITION_CONTEXT('part definition',#10722,'design');
#10695=PRODUCT_DEFINITION('Left_Rod','Left_Rod',#10706,#10687);
#10706=PRODUCT_DEFINITION_FORMATION('',$,#10731);
#10722=APPLICATION_CONTEXT(
'Core Data for Automotive Mechanical Design Process');
#10723=PRODUCT_CONTEXT('part definition',#10722,'mechanical');
#10731=PRODUCT('Left_Rod','Left_Rod',$,(#10723));
#10784=COLOUR_RGB('Grey',0.48,0.52,0.57);
#10785=FILL_AREA_STYLE_COLOUR('',#10784);
#10786=FILL_AREA_STYLE('',(#10785));
#10787=SURFACE_STYLE_FILL_AREA(#10786);
#10788=SURFACE_SIDE_STYLE('',(#10787));
#10789=SURFACE_STYLE_USAGE(.BOTH.,#10788);
#10790=PRESENTATION_STYLE_ASSIGNMENT((#10789));
ENDSEC;
END-ISO-10303-21;
